ISO-10303-21;
HEADER;
/* Generated by software containing ST-Developer
 * from STEP Tools, Inc. (www.steptools.com) 
 */

FILE_DESCRIPTION(
/* description */ ('Bearing housing with oil seal and end cap'),
/* implementation_level */ '2;1');

FILE_NAME(
/* name */ 'Socket Set Screw - M5x8.step',
/* time_stamp */ '2026-10-28T03:23:10-07:00',
/* author */ (''),
/* organization */ (''),
/* preprocessor_version */ 'ST-DEVELOPER v20.2',
/* originating_system */ 'Autodesk Translation Framework v15.17.0.0',
/* authorisation */ '');

FILE_SCHEMA (('AUTOMOTIVE_DESIGN { 1 0 10303 214 3 1 1 }'));
ENDSEC;

DATA;
#10=MECHANICAL_DESIGN_GEOMETRIC_PRESENTATION_REPRESENTATION('',(#287),#7871);
#213=CONICAL_SURFACE('',#4864,0.235,0.785398163397448);
#214=CONICAL_SURFACE('',#4868,0.2125,0.785398163397448);
#237=SHAPE_REPRESENTATION_RELATIONSHIP('SRR','None',#7986,#258);
#258=ADVANCED_BREP_SHAPE_REPRESENTATION('',(#314),#7870);
#287=STYLED_ITEM('',(#8160),#314);
#314=MANIFOLD_SOLID_BREP('Body1',#4115);
#407=FACE_BOUND('',#1142,.T.);
#543=PLANE('',#4855);
#544=PLANE('',#4856);
#545=PLANE('',#4857);
#546=PLANE('',#4858);
#547=PLANE('',#4859);
#548=PLANE('',#4860);
#549=PLANE('',#4861);
#550=PLANE('',#4862);
#551=PLANE('',#4870);
#791=FACE_OUTER_BOUND('',#1134,.T.);
#792=FACE_OUTER_BOUND('',#1135,.T.);
#793=FACE_OUTER_BOUND('',#1136,.T.);
#794=FACE_OUTER_BOUND('',#1137,.T.);
#795=FACE_OUTER_BOUND('',#1138,.T.);
#796=FACE_OUTER_BOUND('',#1139,.T.);
#797=FACE_OUTER_BOUND('',#1140,.T.);
#798=FACE_OUTER_BOUND('',#1141,.T.);
#799=FACE_OUTER_BOUND('',#1143,.T.);
#800=FACE_OUTER_BOUND('',#1144,.T.);
#801=FACE_OUTER_BOUND('',#1145,.T.);
#802=FACE_OUTER_BOUND('',#1146,.T.);
#1134=EDGE_LOOP('',(#3709,#3710,#3711,#3712));
#1135=EDGE_LOOP('',(#3713,#3714,#3715,#3716));
#1136=EDGE_LOOP('',(#3717,#3718,#3719,#3720));
#1137=EDGE_LOOP('',(#3721,#3722,#3723,#3724));
#1138=EDGE_LOOP('',(#3725,#3726,#3727,#3728));
#1139=EDGE_LOOP('',(#3729,#3730,#3731,#3732));
#1140=EDGE_LOOP('',(#3733,#3734,#3735,#3736,#3737,#3738));
#1141=EDGE_LOOP('',(#3739));
#1142=EDGE_LOOP('',(#3740,#3741,#3742,#3743,#3744,#3745));
#1143=EDGE_LOOP('',(#3746,#3747,#3748,#3749));
#1144=EDGE_LOOP('',(#3750,#3751,#3752,#3753));
#1145=EDGE_LOOP('',(#3754,#3755,#3756,#3757));
#1146=EDGE_LOOP('',(#3758));
#1388=LINE('',#7761,#1650);
#1389=LINE('',#7763,#1651);
#1390=LINE('',#7765,#1652);
#1391=LINE('',#7766,#1653);
#1392=LINE('',#7769,#1654);
#1393=LINE('',#7771,#1655);
#1394=LINE('',#7772,#1656);
#1395=LINE('',#7775,#1657);
#1396=LINE('',#7777,#1658);
#1397=LINE('',#7778,#1659);
#1398=LINE('',#7781,#1660);
#1399=LINE('',#7783,#1661);
#1400=LINE('',#7784,#1662);
#1401=LINE('',#7787,#1663);
#1402=LINE('',#7789,#1664);
#1403=LINE('',#7790,#1665);
#1404=LINE('',#7792,#1666);
#1405=LINE('',#7793,#1667);
#1406=LINE('',#7801,#1668);
#1407=LINE('',#7805,#1669);
#1408=LINE('',#7809,#1670);
#1650=VECTOR('',#6137,1.);
#1651=VECTOR('',#6138,1.);
#1652=VECTOR('',#6139,1.);
#1653=VECTOR('',#6140,1.);
#1654=VECTOR('',#6143,1.);
#1655=VECTOR('',#6144,1.);
#1656=VECTOR('',#6145,1.);
#1657=VECTOR('',#6148,1.);
#1658=VECTOR('',#6149,1.);
#1659=VECTOR('',#6150,1.);
#1660=VECTOR('',#6153,1.);
#1661=VECTOR('',#6154,1.);
#1662=VECTOR('',#6155,1.);
#1663=VECTOR('',#6158,1.);
#1664=VECTOR('',#6159,1.);
#1665=VECTOR('',#6160,1.);
#1666=VECTOR('',#6163,1.);
#1667=VECTOR('',#6164,1.);
#1668=VECTOR('',#6175,0.235);
#1669=VECTOR('',#6180,0.25);
#1670=VECTOR('',#6185,0.2125);
#1887=CIRCLE('',#4863,0.22);
#1888=CIRCLE('',#4865,0.24505);
#1889=CIRCLE('',#4867,0.24505);
#1890=CIRCLE('',#4869,0.175);
#2219=VERTEX_POINT('',#7759);
#2220=VERTEX_POINT('',#7760);
#2221=VERTEX_POINT('',#7762);
#2222=VERTEX_POINT('',#7764);
#2223=VERTEX_POINT('',#7768);
#2224=VERTEX_POINT('',#7770);
#2225=VERTEX_POINT('',#7774);
#2226=VERTEX_POINT('',#7776);
#2227=VERTEX_POINT('',#7780);
#2228=VERTEX_POINT('',#7782);
#2229=VERTEX_POINT('',#7786);
#2230=VERTEX_POINT('',#7788);
#2231=VERTEX_POINT('',#7796);
#2232=VERTEX_POINT('',#7799);
#2233=VERTEX_POINT('',#7803);
#2234=VERTEX_POINT('',#7807);
#2718=EDGE_CURVE('',#2219,#2220,#1388,.T.);
#2719=EDGE_CURVE('',#2219,#2221,#1389,.T.);
#2720=EDGE_CURVE('',#2221,#2222,#1390,.T.);
#2721=EDGE_CURVE('',#2220,#2222,#1391,.T.);
#2722=EDGE_CURVE('',#2223,#2219,#1392,.T.);
#2723=EDGE_CURVE('',#2223,#2224,#1393,.T.);
#2724=EDGE_CURVE('',#2224,#2221,#1394,.T.);
#2725=EDGE_CURVE('',#2225,#2223,#1395,.T.);
#2726=EDGE_CURVE('',#2225,#2226,#1396,.T.);
#2727=EDGE_CURVE('',#2226,#2224,#1397,.T.);
#2728=EDGE_CURVE('',#2227,#2225,#1398,.T.);
#2729=EDGE_CURVE('',#2227,#2228,#1399,.T.);
#2730=EDGE_CURVE('',#2228,#2226,#1400,.T.);
#2731=EDGE_CURVE('',#2229,#2227,#1401,.T.);
#2732=EDGE_CURVE('',#2229,#2230,#1402,.T.);
#2733=EDGE_CURVE('',#2230,#2228,#1403,.T.);
#2734=EDGE_CURVE('',#2220,#2229,#1404,.T.);
#2735=EDGE_CURVE('',#2222,#2230,#1405,.T.);
#2736=EDGE_CURVE('',#2231,#2231,#1887,.T.);
#2737=EDGE_CURVE('',#2232,#2232,#1888,.T.);
#2738=EDGE_CURVE('',#2232,#2231,#1406,.T.);
#2739=EDGE_CURVE('',#2233,#2233,#1889,.F.);
#2740=EDGE_CURVE('',#2233,#2232,#1407,.T.);
#2741=EDGE_CURVE('',#2234,#2234,#1890,.T.);
#2742=EDGE_CURVE('',#2234,#2233,#1408,.T.);
#3709=ORIENTED_EDGE('',*,*,#2718,.F.);
#3710=ORIENTED_EDGE('',*,*,#2719,.T.);
#3711=ORIENTED_EDGE('',*,*,#2720,.T.);
#3712=ORIENTED_EDGE('',*,*,#2721,.F.);
#3713=ORIENTED_EDGE('',*,*,#2722,.F.);
#3714=ORIENTED_EDGE('',*,*,#2723,.T.);
#3715=ORIENTED_EDGE('',*,*,#2724,.T.);
#3716=ORIENTED_EDGE('',*,*,#2719,.F.);
#3717=ORIENTED_EDGE('',*,*,#2725,.F.);
#3718=ORIENTED_EDGE('',*,*,#2726,.T.);
#3719=ORIENTED_EDGE('',*,*,#2727,.T.);
#3720=ORIENTED_EDGE('',*,*,#2723,.F.);
#3721=ORIENTED_EDGE('',*,*,#2728,.F.);
#3722=ORIENTED_EDGE('',*,*,#2729,.T.);
#3723=ORIENTED_EDGE('',*,*,#2730,.T.);
#3724=ORIENTED_EDGE('',*,*,#2726,.F.);
#3725=ORIENTED_EDGE('',*,*,#2731,.F.);
#3726=ORIENTED_EDGE('',*,*,#2732,.T.);
#3727=ORIENTED_EDGE('',*,*,#2733,.T.);
#3728=ORIENTED_EDGE('',*,*,#2729,.F.);
#3729=ORIENTED_EDGE('',*,*,#2734,.F.);
#3730=ORIENTED_EDGE('',*,*,#2721,.T.);
#3731=ORIENTED_EDGE('',*,*,#2735,.T.);
#3732=ORIENTED_EDGE('',*,*,#2732,.F.);
#3733=ORIENTED_EDGE('',*,*,#2735,.F.);
#3734=ORIENTED_EDGE('',*,*,#2720,.F.);
#3735=ORIENTED_EDGE('',*,*,#2724,.F.);
#3736=ORIENTED_EDGE('',*,*,#2727,.F.);
#3737=ORIENTED_EDGE('',*,*,#2730,.F.);
#3738=ORIENTED_EDGE('',*,*,#2733,.F.);
#3739=ORIENTED_EDGE('',*,*,#2736,.F.);
#3740=ORIENTED_EDGE('',*,*,#2718,.T.);
#3741=ORIENTED_EDGE('',*,*,#2734,.T.);
#3742=ORIENTED_EDGE('',*,*,#2731,.T.);
#3743=ORIENTED_EDGE('',*,*,#2728,.T.);
#3744=ORIENTED_EDGE('',*,*,#2725,.T.);
#3745=ORIENTED_EDGE('',*,*,#2722,.T.);
#3746=ORIENTED_EDGE('',*,*,#2737,.F.);
#3747=ORIENTED_EDGE('',*,*,#2738,.T.);
#3748=ORIENTED_EDGE('',*,*,#2736,.T.);
#3749=ORIENTED_EDGE('',*,*,#2738,.F.);
#3750=ORIENTED_EDGE('',*,*,#2739,.F.);
#3751=ORIENTED_EDGE('',*,*,#2740,.T.);
#3752=ORIENTED_EDGE('',*,*,#2737,.T.);
#3753=ORIENTED_EDGE('',*,*,#2740,.F.);
#3754=ORIENTED_EDGE('',*,*,#2741,.F.);
#3755=ORIENTED_EDGE('',*,*,#2742,.T.);
#3756=ORIENTED_EDGE('',*,*,#2739,.T.);
#3757=ORIENTED_EDGE('',*,*,#2742,.F.);
#3758=ORIENTED_EDGE('',*,*,#2741,.T.);
#3833=CYLINDRICAL_SURFACE('',#4866,0.24505);
#4073=ADVANCED_FACE('',(#791),#543,.F.);
#4074=ADVANCED_FACE('',(#792),#544,.F.);
#4075=ADVANCED_FACE('',(#793),#545,.F.);
#4076=ADVANCED_FACE('',(#794),#546,.F.);
#4077=ADVANCED_FACE('',(#795),#547,.F.);
#4078=ADVANCED_FACE('',(#796),#548,.F.);
#4079=ADVANCED_FACE('',(#797),#549,.F.);
#4080=ADVANCED_FACE('',(#798,#407),#550,.T.);
#4081=ADVANCED_FACE('',(#799),#213,.T.);
#4082=ADVANCED_FACE('',(#800),#3833,.T.);
#4083=ADVANCED_FACE('',(#801),#214,.T.);
#4084=ADVANCED_FACE('',(#802),#551,.T.);
#4115=CLOSED_SHELL('',(#4073,#4074,#4075,#4076,#4077,#4078,#4079,#4080,
#4081,#4082,#4083,#4084));
#4854=AXIS2_PLACEMENT_3D('',#7757,#6133,#6134);
#4855=AXIS2_PLACEMENT_3D('',#7758,#6135,#6136);
#4856=AXIS2_PLACEMENT_3D('',#7767,#6141,#6142);
#4857=AXIS2_PLACEMENT_3D('',#7773,#6146,#6147);
#4858=AXIS2_PLACEMENT_3D('',#7779,#6151,#6152);
#4859=AXIS2_PLACEMENT_3D('',#7785,#6156,#6157);
#4860=AXIS2_PLACEMENT_3D('',#7791,#6161,#6162);
#4861=AXIS2_PLACEMENT_3D('',#7794,#6165,#6166);
#4862=AXIS2_PLACEMENT_3D('',#7795,#6167,#6168);
#4863=AXIS2_PLACEMENT_3D('',#7797,#6169,#6170);
#4864=AXIS2_PLACEMENT_3D('',#7798,#6171,#6172);
#4865=AXIS2_PLACEMENT_3D('',#7800,#6173,#6174);
#4866=AXIS2_PLACEMENT_3D('',#7802,#6176,#6177);
#4867=AXIS2_PLACEMENT_3D('',#7804,#6178,#6179);
#4868=AXIS2_PLACEMENT_3D('',#7806,#6181,#6182);
#4869=AXIS2_PLACEMENT_3D('',#7808,#6183,#6184);
#4870=AXIS2_PLACEMENT_3D('',#7810,#6186,#6187);
#6133=DIRECTION('axis',(0.,0.,1.));
#6134=DIRECTION('refdir',(1.,0.,0.));
#6135=DIRECTION('center_axis',(0.866025403784439,0.,-0.5));
#6136=DIRECTION('ref_axis',(0.5,0.,0.866025403784439));
#6137=DIRECTION('',(0.5,0.,0.866025403784439));
#6138=DIRECTION('',(0.,-1.,0.));
#6139=DIRECTION('',(0.5,0.,0.866025403784439));
#6140=DIRECTION('',(0.,-1.,0.));
#6141=DIRECTION('center_axis',(1.92296268638356E-16,0.,-1.));
#6142=DIRECTION('ref_axis',(1.,0.,1.92296268638356E-16));
#6143=DIRECTION('',(1.,0.,1.92296268638356E-16));
#6144=DIRECTION('',(0.,-1.,0.));
#6145=DIRECTION('',(1.,0.,1.92296268638356E-16));
#6146=DIRECTION('center_axis',(-0.866025403784439,0.,-0.5));
#6147=DIRECTION('ref_axis',(0.5,0.,-0.866025403784439));
#6148=DIRECTION('',(0.5,0.,-0.866025403784439));
#6149=DIRECTION('',(0.,-1.,0.));
#6150=DIRECTION('',(0.5,0.,-0.866025403784438));
#6151=DIRECTION('center_axis',(-0.866025403784439,0.,0.5));
#6152=DIRECTION('ref_axis',(-0.5,0.,-0.866025403784439));
#6153=DIRECTION('',(-0.5,0.,-0.866025403784439));
#6154=DIRECTION('',(0.,-1.,0.));
#6155=DIRECTION('',(-0.5,0.,-0.866025403784439));
#6156=DIRECTION('center_axis',(-1.92296268638356E-16,0.,1.));
#6157=DIRECTION('ref_axis',(-1.,0.,-1.92296268638356E-16));
#6158=DIRECTION('',(-1.,0.,-1.92296268638356E-16));
#6159=DIRECTION('',(0.,-1.,0.));
#6160=DIRECTION('',(-1.,0.,-1.92296268638356E-16));
#6161=DIRECTION('center_axis',(0.866025403784439,0.,0.5));
#6162=DIRECTION('ref_axis',(-0.5,0.,0.866025403784439));
#6163=DIRECTION('',(-0.5,0.,0.866025403784439));
#6164=DIRECTION('',(-0.5,0.,0.866025403784439));
#6165=DIRECTION('center_axis',(0.,-1.,0.));
#6166=DIRECTION('ref_axis',(0.,0.,-1.));
#6167=DIRECTION('center_axis',(0.,1.,0.));
#6168=DIRECTION('ref_axis',(0.,0.,1.));
#6169=DIRECTION('center_axis',(0.,-1.,0.));
#6170=DIRECTION('ref_axis',(1.,0.,0.));
#6171=DIRECTION('center_axis',(0.,-1.,0.));
#6172=DIRECTION('ref_axis',(1.,0.,0.));
#6173=DIRECTION('center_axis',(0.,-1.,0.));
#6174=DIRECTION('ref_axis',(1.,0.,0.));
#6175=DIRECTION('',(0.707106781186547,0.707106781186548,8.65956056235493E-17));
#6176=DIRECTION('center_axis',(0.,-1.,0.));
#6177=DIRECTION('ref_axis',(1.,0.,0.));
#6178=DIRECTION('center_axis',(0.,1.,0.));
#6179=DIRECTION('ref_axis',(1.,0.,0.));
#6180=DIRECTION('',(0.,1.,0.));
#6181=DIRECTION('center_axis',(0.,1.,0.));
#6182=DIRECTION('ref_axis',(1.,0.,0.));
#6183=DIRECTION('center_axis',(0.,-1.,0.));
#6184=DIRECTION('ref_axis',(1.,0.,0.));
#6185=DIRECTION('',(-0.707106781186547,0.707106781186548,-8.65956056235493E-17));
#6186=DIRECTION('center_axis',(0.,-1.,0.));
#6187=DIRECTION('ref_axis',(0.,0.,-1.));
#7757=CARTESIAN_POINT('',(0.,0.,0.));
#7758=CARTESIAN_POINT('Origin',(0.0721687836487032,0.,-0.125));
#7759=CARTESIAN_POINT('',(0.0721687836487032,0.,-0.125));
#7760=CARTESIAN_POINT('',(0.144337567297406,0.,0.));
#7761=CARTESIAN_POINT('',(0.117710979560879,0.,-0.0461186027918559));
#7762=CARTESIAN_POINT('',(0.0721687836487032,-0.25,-0.125));
#7763=CARTESIAN_POINT('',(0.0721687836487032,0.,-0.125));
#7764=CARTESIAN_POINT('',(0.144337567297406,-0.25,0.));
#7765=CARTESIAN_POINT('',(0.144337567297406,-0.25,0.));
#7766=CARTESIAN_POINT('',(0.144337567297406,0.,0.));
#7767=CARTESIAN_POINT('Origin',(-0.0721687836487032,0.,-0.125));
#7768=CARTESIAN_POINT('',(-0.0721687836487032,0.,-0.125));
#7769=CARTESIAN_POINT('',(0.0739156081756484,0.,-0.125));
#7770=CARTESIAN_POINT('',(-0.0721687836487032,-0.25,-0.125));
#7771=CARTESIAN_POINT('',(-0.0721687836487032,0.,-0.125));
#7772=CARTESIAN_POINT('',(0.0721687836487032,-0.25,-0.125));
#7773=CARTESIAN_POINT('Origin',(-0.144337567297406,0.,-4.16333634234434E-17));
#7774=CARTESIAN_POINT('',(-0.144337567297406,0.,-1.76762539787485E-17));
#7775=CARTESIAN_POINT('',(-0.0987953713852306,0.,-0.0788813972081442));
#7776=CARTESIAN_POINT('',(-0.144337567297406,-0.25,-2.77555756156289E-17));
#7777=CARTESIAN_POINT('',(-0.144337567297406,0.,-1.76762539787485E-17));
#7778=CARTESIAN_POINT('',(-0.0721687836487032,-0.25,-0.125));
#7779=CARTESIAN_POINT('Origin',(-0.0721687836487033,0.,0.125));
#7780=CARTESIAN_POINT('',(-0.0721687836487033,0.,0.125));
#7781=CARTESIAN_POINT('',(-0.0627109795608791,0.,0.141381397208144));
#7782=CARTESIAN_POINT('',(-0.0721687836487033,-0.25,0.125));
#7783=CARTESIAN_POINT('',(-0.0721687836487033,0.,0.125));
#7784=CARTESIAN_POINT('',(-0.144337567297406,-0.25,-1.76762539787485E-17));
#7785=CARTESIAN_POINT('Origin',(0.0721687836487032,0.,0.125));
#7786=CARTESIAN_POINT('',(0.0721687836487032,0.,0.125));
#7787=CARTESIAN_POINT('',(0.146084391824352,0.,0.125));
#7788=CARTESIAN_POINT('',(0.0721687836487032,-0.25,0.125));
#7789=CARTESIAN_POINT('',(0.0721687836487032,0.,0.125));
#7790=CARTESIAN_POINT('',(-0.0721687836487033,-0.25,0.125));
#7791=CARTESIAN_POINT('Origin',(0.144337567297406,0.,0.));
#7792=CARTESIAN_POINT('',(0.153795371385231,0.,-0.0163813972081441));
#7793=CARTESIAN_POINT('',(0.0721687836487032,-0.25,0.125));
#7794=CARTESIAN_POINT('Origin',(0.,-0.25,0.));
#7795=CARTESIAN_POINT('Origin',(0.22,0.,0.));
#7796=CARTESIAN_POINT('',(-0.22,-8.67361737988404E-18,-2.69422295812418E-17));
#7797=CARTESIAN_POINT('Origin',(0.,0.,0.));
#7798=CARTESIAN_POINT('Origin',(0.,-0.015,0.));
#7799=CARTESIAN_POINT('',(-0.24505,-0.02505,-3.00099698131059E-17));
#7800=CARTESIAN_POINT('Origin',(0.,-0.02505,0.));
#7801=CARTESIAN_POINT('',(-0.235,-0.015,-2.87791997799628E-17));
#7802=CARTESIAN_POINT('Origin',(0.,-0.3775,0.));
#7803=CARTESIAN_POINT('',(-0.24505,-0.72995,3.00099698131059E-17));
#7804=CARTESIAN_POINT('Origin',(0.,-0.72995,0.));
#7805=CARTESIAN_POINT('',(-0.24505,-0.3775,-3.00099698131059E-17));
#7806=CARTESIAN_POINT('Origin',(0.,-0.7625,0.));
#7807=CARTESIAN_POINT('',(-0.175,-0.8,-2.14313189850787E-17));
#7808=CARTESIAN_POINT('Origin',(0.,-0.8,0.));
#7809=CARTESIAN_POINT('',(-0.2125,-0.7625,-2.60237444818813E-17));
#7810=CARTESIAN_POINT('Origin',(0.,-0.8,0.));
#7844=UNCERTAINTY_MEASURE_WITH_UNIT(LENGTH_MEASURE(0.001),#7872,
'DISTANCE_ACCURACY_VALUE',
'Maximum model space distance between geometric entities at asserted c
onnectivities');
#7845=UNCERTAINTY_MEASURE_WITH_UNIT(LENGTH_MEASURE(0.001),#7872,
'DISTANCE_ACCURACY_VALUE',
'Maximum model space distance between geometric entities at asserted c
onnectivities');
#7870=(
GEOMETRIC_REPRESENTATION_CONTEXT(3)
GLOBAL_UNCERTAINTY_ASSIGNED_CONTEXT((#7844))
GLOBAL_UNIT_ASSIGNED_CONTEXT((#7872,#7874,#7875))
REPRESENTATION_CONTEXT('','3D')
);
#7871=(
GEOMETRIC_REPRESENTATION_CONTEXT(3)
GLOBAL_UNCERTAINTY_ASSIGNED_CONTEXT((#7845))
GLOBAL_UNIT_ASSIGNED_CONTEXT((#7872,#7874,#7875))
REPRESENTATION_CONTEXT('','3D')
);
#7872=(
LENGTH_UNIT()
NAMED_UNIT(*)
SI_UNIT(.CENTI.,.METRE.)
);
#7874=(
NAMED_UNIT(*)
PLANE_ANGLE_UNIT()
SI_UNIT($,.RADIAN.)
);
#7875=(
NAMED_UNIT(*)
SI_UNIT($,.STERADIAN.)
SOLID_ANGLE_UNIT()
);
#7900=SHAPE_DEFINITION_REPRESENTATION(#7952,#7986);
#7952=PRODUCT_DEFINITION_SHAPE('',$,#8012);
#7986=SHAPE_REPRESENTATION('',(#4854),#7870);
#7987=PRODUCT_DEFINITION_CONTEXT('part definition',#8064,'design');
#8012=PRODUCT_DEFINITION('Socket Set Screw - M5x8',
'Socket Set Screw - M5x8',#8037,#7987);
#8037=PRODUCT_DEFINITION_FORMATION('',$,#8090);
#8064=APPLICATION_CONTEXT(
'Core Data for Automotive Mechanical Design Process');
#8065=PRODUCT_CONTEXT('part definition',#8064,'mechanical');
#8090=PRODUCT('Socket Set Screw - M5x8','Socket Set Screw - M5x8',
'Socket Set Screw - M5x8',(#8065));
#8154=COLOUR_RGB('Black',0.12,0.14,0.17);
#8155=FILL_AREA_STYLE_COLOUR('',#8154);
#8156=FILL_AREA_STYLE('',(#8155));
#8157=SURFACE_STYLE_FILL_AREA(#8156);
#8158=SURFACE_SIDE_STYLE('',(#8157));
#8159=SURFACE_STYLE_USAGE(.BOTH.,#8158);
#8160=PRESENTATION_STYLE_ASSIGNMENT((#8159));
ENDSEC;
END-ISO-10303-21;
